ISO-10303-21;
HEADER;
FILE_DESCRIPTION (('STEP AP214'),
    '1' );
FILE_NAME ('nut M10.step',
    '2026-10-06T07:34:29',
    ( '' ),
    ( '' ),
    'SwSTEP 2.0',
    'SolidWorks 2025',
    '' );
FILE_SCHEMA (( 'AUTOMOTIVE_DESIGN' ));
ENDSEC;

DATA;
#18=MECHANICAL_DESIGN_GEOMETRIC_PRESENTATION_REPRESENTATION('',(#1288),#7370);
#53=PLANE ( 'NONE',  #11171 ) ;
#124=FACE_OUTER_BOUND ( 'NONE', #1519, .T. ) ;
#125=LINE ( 'NONE', #13401, #6173 ) ;
#135=ADVANCED_FACE ( 'NONE', ( #124, #11996 ), #53, .F. ) ;
#195=DIRECTION ( 'NONE',  ( 1.000000000000000000, 0.000000000000000000, -0.000000000000000000 ) ) ;
#286=AXIS2_PLACEMENT_3D ( 'NONE', #9137, #2973, #11498 ) ;
#408=ORIENTED_EDGE ( 'NONE', *, *, #12361, .F. ) ;
#434=DIRECTION ( 'NONE',  ( 1.000000000000000000, 0.000000000000000000, 0.000000000000000000 ) ) ;
#513=ADVANCED_FACE ( 'NONE', ( #9255 ), #2959, .F. ) ;
#562=LINE ( 'NONE', #5161, #14608 ) ;
#563=MANIFOLD_SOLID_BREP ( 'Boss-Extrude1', #14676 ) ;
#604=PRODUCT_DEFINITION_CONTEXT ( 'detailed design', #12686, 'design' ) ;
#645=VERTEX_POINT ( 'NONE', #14203 ) ;
#684=ORIENTED_EDGE ( 'NONE', *, *, #4682, .F. ) ;
#704=PRODUCT_DEFINITION_FORMATION_WITH_SPECIFIED_SOURCE ( 'ANY', '', #10548, .NOT_KNOWN. ) ;
#812=DIRECTION ( 'NONE',  ( -1.000000000000000000, -1.669238443041287429E-16, 0.000000000000000000 ) ) ;
#852=ORIENTED_EDGE ( 'NONE', *, *, #6243, .T. ) ;
#857=LINE ( 'NONE', #5690, #11930 ) ;
#927=VERTEX_POINT ( 'NONE', #8374 ) ;
#948=EDGE_CURVE ( 'NONE', #14543, #645, #2118, .T. ) ;
#971=DIRECTION ( 'NONE',  ( 0.000000000000000000, -0.000000000000000000, 1.000000000000000000 ) ) ;
#1032=DIRECTION ( 'NONE',  ( 0.8660254037844385966, 0.5000000000000001110, -0.000000000000000000 ) ) ;
#1061=( LENGTH_UNIT ( ) NAMED_UNIT ( * ) SI_UNIT ( .MILLI., .METRE. ) );
#1067=DIRECTION ( 'NONE',  ( 0.000000000000000000, 0.000000000000000000, 1.000000000000000000 ) ) ;
#1257=ORIENTED_EDGE ( 'NONE', *, *, #4917, .T. ) ;
#1288=STYLED_ITEM ( 'NONE', ( #11699 ), #563 ) ;
#1306=CARTESIAN_POINT ( 'NONE',  ( 5.000000000000000000, 6.123233995736766282E-16, 5.000000000000000000 ) ) ;
#1328=VERTEX_POINT ( 'NONE', #15343 ) ;
#1361=FACE_OUTER_BOUND ( 'NONE', #1656, .T. ) ;
#1440=ORIENTED_EDGE ( 'NONE', *, *, #5443, .T. ) ;
#1453=CARTESIAN_POINT ( 'NONE',  ( 0.000000000000000000, 0.000000000000000000, 5.000000000000000000 ) ) ;
#1519=EDGE_LOOP ( 'NONE', ( #9319, #15000, #14239, #408, #11238, #5624 ) ) ;
#1533=EDGE_LOOP ( 'NONE', ( #9557, #1537, #3772, #14772 ) ) ;
#1537=ORIENTED_EDGE ( 'NONE', *, *, #12204, .F. ) ;
#1540=LINE ( 'NONE', #2735, #7744 ) ;
#1652=EDGE_LOOP ( 'NONE', ( #1257, #1825, #15285, #1440 ) ) ;
#1656=EDGE_LOOP ( 'NONE', ( #3101, #4886, #14421, #13016 ) ) ;
#1670=EDGE_CURVE ( 'NONE', #9409, #14543, #3028, .T. ) ;
#1708=CARTESIAN_POINT ( 'NONE',  ( -5.196152422706630247, -9.000000000000005329, 5.000000000000000000 ) ) ;
#1735=CIRCLE ( 'NONE', #12316, 5.000000000000000000 ) ;
#1747=ORIENTED_EDGE ( 'NONE', *, *, #9225, .F. ) ;
#1825=ORIENTED_EDGE ( 'NONE', *, *, #7680, .F. ) ;
#1827=CARTESIAN_POINT ( 'NONE',  ( 10.39230484541326582, 0.000000000000000000, 0.000000000000000000 ) ) ;
#1863=EDGE_LOOP ( 'NONE', ( #13669, #11225 ) ) ;
#1878=ADVANCED_FACE ( 'NONE', ( #12879 ), #4591, .F. ) ;
#1949=VECTOR ( 'NONE', #2753, 1000.000000000000114 ) ;
#2021=VECTOR ( 'NONE', #6436, 1000.000000000000114 ) ;
#2115=DIRECTION ( 'NONE',  ( -1.000000000000000000, 0.000000000000000000, 0.000000000000000000 ) ) ;
#2118=LINE ( 'NONE', #10726, #5858 ) ;
#2138=ORIENTED_EDGE ( 'NONE', *, *, #3221, .T. ) ;
#2223=EDGE_CURVE ( 'NONE', #8472, #9409, #2698, .T. ) ;
#2305=DIRECTION ( 'NONE',  ( -0.4999999999999997224, -0.8660254037844387076, 0.000000000000000000 ) ) ;
#2398=ORIENTED_EDGE ( 'NONE', *, *, #14658, .T. ) ;
#2452=FACE_OUTER_BOUND ( 'NONE', #3286, .T. ) ;
#2467=EDGE_LOOP ( 'NONE', ( #14037, #4593 ) ) ;
#2521=VECTOR ( 'NONE', #8962, 1000.000000000000000 ) ;
#2579=ORIENTED_EDGE ( 'NONE', *, *, #10572, .T. ) ;
#2698=LINE ( 'NONE', #7517, #5304 ) ;
#2735=CARTESIAN_POINT ( 'NONE',  ( -5.196152422706636465, 9.000000000000001776, 5.000000000000000000 ) ) ;
#2753=DIRECTION ( 'NONE',  ( 0.5000000000000001110, -0.8660254037844385966, 0.000000000000000000 ) ) ;
#2787=LINE ( 'NONE', #11078, #7974 ) ;
#2851=CIRCLE ( 'NONE', #4345, 5.000000000000000000 ) ;
#2853=ORIENTED_EDGE ( 'NONE', *, *, #5443, .F. ) ;
#2959=PLANE ( 'NONE',  #4066 ) ;
#2973=DIRECTION ( 'NONE',  ( 0.000000000000000000, 0.000000000000000000, 1.000000000000000000 ) ) ;
#2996=EDGE_CURVE ( 'NONE', #13828, #3648, #1540, .T. ) ;
#3028=LINE ( 'NONE', #15083, #2021 ) ;
#3101=ORIENTED_EDGE ( 'NONE', *, *, #3843, .T. ) ;
#3123=DIRECTION ( 'NONE',  ( 1.000000000000000000, 0.000000000000000000, -0.000000000000000000 ) ) ;
#3210=LINE ( 'NONE', #6631, #6763 ) ;
#3221=EDGE_CURVE ( 'NONE', #13828, #11543, #6612, .T. ) ;
#3276=LINE ( 'NONE', #11800, #15341 ) ;
#3286=EDGE_LOOP ( 'NONE', ( #3980, #9995, #684, #12442 ) ) ;
#3392=VECTOR ( 'NONE', #4174, 1000.000000000000000 ) ;
#3432=FACE_OUTER_BOUND ( 'NONE', #12476, .T. ) ;
#3487=DIRECTION ( 'NONE',  ( -0.8660254037844388186, 0.4999999999999997780, 0.000000000000000000 ) ) ;
#3508=ADVANCED_FACE ( 'NONE', ( #1361 ), #10060, .F. ) ;
#3591=SHAPE_DEFINITION_REPRESENTATION ( #11691, #12546 ) ;
#3607=LINE ( 'NONE', #1306, #9183 ) ;
#3648=VERTEX_POINT ( 'NONE', #4357 ) ;
#3734=DIRECTION ( 'NONE',  ( -0.000000000000000000, -0.000000000000000000, -1.000000000000000000 ) ) ;
#3772=ORIENTED_EDGE ( 'NONE', *, *, #3221, .F. ) ;
#3843=EDGE_CURVE ( 'NONE', #9433, #645, #4118, .T. ) ;
#3971=( NAMED_UNIT ( * ) PLANE_ANGLE_UNIT ( ) SI_UNIT ( $, .RADIAN. ) );
#3980=ORIENTED_EDGE ( 'NONE', *, *, #4833, .T. ) ;
#3987=CARTESIAN_POINT ( 'NONE',  ( -10.39230484541326582, 4.570335331080236228E-16, 5.000000000000000000 ) ) ;
#4041=CARTESIAN_POINT ( 'NONE',  ( -5.000000000000000000, 0.000000000000000000, 5.000000000000000000 ) ) ;
#4066=AXIS2_PLACEMENT_3D ( 'NONE', #8081, #14859, #12866 ) ;
#4109=ADVANCED_FACE ( 'NONE', ( #2452 ), #8402, .F. ) ;
#4118=LINE ( 'NONE', #1827, #10308 ) ;
#4153=EDGE_LOOP ( 'NONE', ( #2579, #5385, #9025, #14054 ) ) ;
#4174=DIRECTION ( 'NONE',  ( -0.000000000000000000, -0.000000000000000000, -1.000000000000000000 ) ) ;
#4249=LINE ( 'NONE', #12625, #3392 ) ;
#4323=FACE_OUTER_BOUND ( 'NONE', #4153, .T. ) ;
#4345=AXIS2_PLACEMENT_3D ( 'NONE', #7917, #13897, #6657 ) ;
#4357=CARTESIAN_POINT ( 'NONE',  ( -5.196152422706636465, 9.000000000000001776, 0.000000000000000000 ) ) ;
#4568=CARTESIAN_POINT ( 'NONE',  ( 0.000000000000000000, 0.000000000000000000, 0.000000000000000000 ) ) ;
#4591=PLANE ( 'NONE',  #6322 ) ;
#4593=ORIENTED_EDGE ( 'NONE', *, *, #14658, .F. ) ;
#4669=FACE_OUTER_BOUND ( 'NONE', #1652, .T. ) ;
#4682=EDGE_CURVE ( 'NONE', #11543, #11731, #4964, .T. ) ;
#4747=PLANE ( 'NONE',  #13417 ) ;
#4749=VERTEX_POINT ( 'NONE', #14576 ) ;
#4833=EDGE_CURVE ( 'NONE', #6413, #9150, #3210, .T. ) ;
#4886=ORIENTED_EDGE ( 'NONE', *, *, #948, .F. ) ;
#4917=EDGE_CURVE ( 'NONE', #4749, #9433, #8133, .T. ) ;
#4964=LINE ( 'NONE', #7655, #1949 ) ;
#4966=CARTESIAN_POINT ( 'NONE',  ( 0.000000000000000000, 0.000000000000000000, 0.000000000000000000 ) ) ;
#4996=DIRECTION ( 'NONE',  ( -0.4999999999999997224, -0.8660254037844388186, 0.000000000000000000 ) ) ;
#5161=CARTESIAN_POINT ( 'NONE',  ( 10.39230484541326582, 0.000000000000000000, 5.000000000000000000 ) ) ;
#5171=EDGE_CURVE ( 'NONE', #11731, #9150, #4249, .T. ) ;
#5237=LINE ( 'NONE', #13755, #2521 ) ;
#5286=CIRCLE ( 'NONE', #7321, 5.000000000000000000 ) ;
#5304=VECTOR ( 'NONE', #12314, 1000.000000000000114 ) ;
#5385=ORIENTED_EDGE ( 'NONE', *, *, #5899, .T. ) ;
#5443=EDGE_CURVE ( 'NONE', #8472, #4749, #125, .T. ) ;
#5506=VECTOR ( 'NONE', #12919, 1000.000000000000114 ) ;
#5530=DIRECTION ( 'NONE',  ( 1.000000000000000000, 1.669238443041287429E-16, 0.000000000000000000 ) ) ;
#5542=ORIENTED_EDGE ( 'NONE', *, *, #2996, .F. ) ;
#5582=EDGE_LOOP ( 'NONE', ( #11889, #2398, #8375, #14553 ) ) ;
#5618=FILL_AREA_STYLE ('',( #10436 ) ) ;
#5624=ORIENTED_EDGE ( 'NONE', *, *, #3843, .F. ) ;
#5681=DIRECTION ( 'NONE',  ( 1.000000000000000000, 0.000000000000000000, 0.000000000000000000 ) ) ;
#5690=CARTESIAN_POINT ( 'NONE',  ( 5.196152422706632024, 9.000000000000003553, 5.000000000000000000 ) ) ;
#5694=( NAMED_UNIT ( * ) SI_UNIT ( $, .STERADIAN. ) SOLID_ANGLE_UNIT ( ) );
#5848=PRODUCT_DEFINITION ( 'UNKNOWN', '', #704, #604 ) ;
#5858=VECTOR ( 'NONE', #14341, 1000.000000000000000 ) ;
#5878=APPLICATION_CONTEXT ( 'automotive_design' ) ;
#5899=EDGE_CURVE ( 'NONE', #927, #11071, #3607, .T. ) ;
#5903=AXIS2_PLACEMENT_3D ( 'NONE', #1453, #12507, #11331 ) ;
#6022=CARTESIAN_POINT ( 'NONE',  ( 5.000000000000000000, 6.123233995736766282E-16, 0.000000000000000000 ) ) ;
#6072=ADVANCED_FACE ( 'NONE', ( #10231 ), #13690, .F. ) ;
#6173=VECTOR ( 'NONE', #9784, 1000.000000000000000 ) ;
#6202=VECTOR ( 'NONE', #15253, 1000.000000000000000 ) ;
#6243=EDGE_CURVE ( 'NONE', #645, #3648, #3276, .T. ) ;
#6322=AXIS2_PLACEMENT_3D ( 'NONE', #6819, #8175, #10519 ) ;
#6379=DIRECTION ( 'NONE',  ( -0.000000000000000000, -0.000000000000000000, -1.000000000000000000 ) ) ;
#6413=VERTEX_POINT ( 'NONE', #7153 ) ;
#6436=DIRECTION ( 'NONE',  ( -0.4999999999999999445, 0.8660254037844385966, 0.000000000000000000 ) ) ;
#6612=LINE ( 'NONE', #10466, #6202 ) ;
#6616=ADVANCED_BREP_SHAPE_REPRESENTATION ( '', ( #563, #12337 ), #9054 ) ;
#6631=CARTESIAN_POINT ( 'NONE',  ( -10.39230484541326582, 4.570335331080236228E-16, 0.000000000000000000 ) ) ;
#6657=DIRECTION ( 'NONE',  ( 1.000000000000000000, 0.000000000000000000, 0.000000000000000000 ) ) ;
#6763=VECTOR ( 'NONE', #6861, 1000.000000000000114 ) ;
#6819=CARTESIAN_POINT ( 'NONE',  ( -5.196152422706636465, 9.000000000000001776, 5.000000000000000000 ) ) ;
#6861=DIRECTION ( 'NONE',  ( 0.5000000000000001110, -0.8660254037844385966, 0.000000000000000000 ) ) ;
#6920=CARTESIAN_POINT ( 'NONE',  ( 0.000000000000000000, 0.000000000000000000, 5.000000000000000000 ) ) ;
#6930=EDGE_CURVE ( 'NONE', #1328, #11071, #5286, .T. ) ;
#6932=CARTESIAN_POINT ( 'NONE',  ( 0.000000000000000000, 0.000000000000000000, 5.000000000000000000 ) ) ;
#6948=VECTOR ( 'NONE', #15549, 1000.000000000000000 ) ;
#7064=LINE ( 'NONE', #11872, #6948 ) ;
#7095=VECTOR ( 'NONE', #10018, 1000.000000000000000 ) ;
#7133=CARTESIAN_POINT ( 'NONE',  ( -10.39230484541326582, 4.570335331080236228E-16, 5.000000000000000000 ) ) ;
#7153=CARTESIAN_POINT ( 'NONE',  ( -10.39230484541326582, 4.570335331080236228E-16, 0.000000000000000000 ) ) ;
#7266=ADVANCED_FACE ( 'NONE', ( #3432, #12818 ), #14080, .T. ) ;
#7321=AXIS2_PLACEMENT_3D ( 'NONE', #11433, #13878, #434 ) ;
#7370=( GEOMETRIC_REPRESENTATION_CONTEXT ( 3 ) GLOBAL_UNCERTAINTY_ASSIGNED_CONTEXT ( ( #15096 ) ) GLOBAL_UNIT_ASSIGNED_CONTEXT ( ( #10146, #3971, #5694 ) ) REPRESENTATION_CONTEXT ( 'NONE', 'WORKASPACE' ) );
#7517=CARTESIAN_POINT ( 'NONE',  ( 5.196152422706635576, -9.000000000000003553, 5.000000000000000000 ) ) ;
#7551=ORIENTED_EDGE ( 'NONE', *, *, #7569, .T. ) ;
#7569=EDGE_CURVE ( 'NONE', #9150, #4749, #5237, .T. ) ;
#7632=ORIENTED_EDGE ( 'NONE', *, *, #2223, .T. ) ;
#7655=CARTESIAN_POINT ( 'NONE',  ( -10.39230484541326582, 4.570335331080236228E-16, 5.000000000000000000 ) ) ;
#7680=EDGE_CURVE ( 'NONE', #9409, #9433, #562, .T. ) ;
#7686=CYLINDRICAL_SURFACE ( 'NONE', #15224, 5.000000000000000000 ) ;
#7744=VECTOR ( 'NONE', #6379, 1000.000000000000000 ) ;
#7816=CARTESIAN_POINT ( 'NONE',  ( 5.196152422706635576, -9.000000000000003553, 0.000000000000000000 ) ) ;
#7917=CARTESIAN_POINT ( 'NONE',  ( 0.000000000000000000, 0.000000000000000000, 0.000000000000000000 ) ) ;
#7974=VECTOR ( 'NONE', #4996, 1000.000000000000000 ) ;
#7983=ADVANCED_FACE ( 'NONE', ( #4669 ), #4747, .F. ) ;
#8081=CARTESIAN_POINT ( 'NONE',  ( -5.196152422706630247, -9.000000000000005329, 5.000000000000000000 ) ) ;
#8123=CARTESIAN_POINT ( 'NONE',  ( 5.196152422706632024, 9.000000000000003553, 5.000000000000000000 ) ) ;
#8133=LINE ( 'NONE', #7816, #5506 ) ;
#8147=DIRECTION ( 'NONE',  ( 0.000000000000000000, 0.000000000000000000, 1.000000000000000000 ) ) ;
#8173=EDGE_CURVE ( 'NONE', #11071, #1328, #2851, .T. ) ;
#8175=DIRECTION ( 'NONE',  ( 0.8660254037844388186, -0.4999999999999997780, 0.000000000000000000 ) ) ;
#8253=EDGE_CURVE ( 'NONE', #14543, #13828, #857, .T. ) ;
#8354=DIRECTION ( 'NONE',  ( 1.000000000000000000, 0.000000000000000000, 0.000000000000000000 ) ) ;
#8374=CARTESIAN_POINT ( 'NONE',  ( 5.000000000000000000, 6.123233995736766282E-16, 5.000000000000000000 ) ) ;
#8375=ORIENTED_EDGE ( 'NONE', *, *, #9637, .T. ) ;
#8402=PLANE ( 'NONE',  #14825 ) ;
#8472=VERTEX_POINT ( 'NONE', #14173 ) ;
#8532=ORIENTED_EDGE ( 'NONE', *, *, #4682, .T. ) ;
#8796=DIRECTION ( 'NONE',  ( -0.8660254037844387076, -0.5000000000000001110, 0.000000000000000000 ) ) ;
#8962=DIRECTION ( 'NONE',  ( 1.000000000000000000, 1.669238443041287922E-16, 0.000000000000000000 ) ) ;
#9025=ORIENTED_EDGE ( 'NONE', *, *, #6930, .F. ) ;
#9054=( GEOMETRIC_REPRESENTATION_CONTEXT ( 3 ) GLOBAL_UNCERTAINTY_ASSIGNED_CONTEXT ( ( #11362 ) ) GLOBAL_UNIT_ASSIGNED_CONTEXT ( ( #1061, #13937, #10701 ) ) REPRESENTATION_CONTEXT ( 'NONE', 'WORKASPACE' ) );
#9064=AXIS2_PLACEMENT_3D ( 'NONE', #6920, #971, #3123 ) ;
#9137=CARTESIAN_POINT ( 'NONE',  ( 0.000000000000000000, 0.000000000000000000, 5.000000000000000000 ) ) ;
#9150=VERTEX_POINT ( 'NONE', #12214 ) ;
#9183=VECTOR ( 'NONE', #9768, 1000.000000000000000 ) ;
#9225=EDGE_CURVE ( 'NONE', #11731, #8472, #13625, .T. ) ;
#9255=FACE_OUTER_BOUND ( 'NONE', #14123, .T. ) ;
#9319=ORIENTED_EDGE ( 'NONE', *, *, #4917, .F. ) ;
#9409=VERTEX_POINT ( 'NONE', #15267 ) ;
#9433=VERTEX_POINT ( 'NONE', #10400 ) ;
#9516=EDGE_LOOP ( 'NONE', ( #852, #5542, #13765, #12559 ) ) ;
#9557=ORIENTED_EDGE ( 'NONE', *, *, #12361, .T. ) ;
#9637=EDGE_CURVE ( 'NONE', #15023, #1328, #10053, .T. ) ;
#9768=DIRECTION ( 'NONE',  ( -0.000000000000000000, -0.000000000000000000, -1.000000000000000000 ) ) ;
#9784=DIRECTION ( 'NONE',  ( -0.000000000000000000, -0.000000000000000000, -1.000000000000000000 ) ) ;
#9988=DIRECTION ( 'NONE',  ( 0.5000000000000000000, -0.8660254037844385966, 0.000000000000000000 ) ) ;
#9989=DIRECTION ( 'NONE',  ( -0.000000000000000000, -0.000000000000000000, -1.000000000000000000 ) ) ;
#9995=ORIENTED_EDGE ( 'NONE', *, *, #5171, .F. ) ;
#10009=ADVANCED_FACE ( 'NONE', ( #15138 ), #12465, .F. ) ;
#10018=DIRECTION ( 'NONE',  ( 1.000000000000000000, 1.669238443041287922E-16, 0.000000000000000000 ) ) ;
#10053=LINE ( 'NONE', #4041, #11378 ) ;
#10060=PLANE ( 'NONE',  #14255 ) ;
#10113=DIRECTION ( 'NONE',  ( 1.669238443041287429E-16, -1.000000000000000000, 0.000000000000000000 ) ) ;
#10146=( LENGTH_UNIT ( ) NAMED_UNIT ( * ) SI_UNIT ( .MILLI., .METRE. ) );
#10231=FACE_OUTER_BOUND ( 'NONE', #5582, .T. ) ;
#10308=VECTOR ( 'NONE', #11083, 1000.000000000000114 ) ;
#10400=CARTESIAN_POINT ( 'NONE',  ( 10.39230484541326582, 0.000000000000000000, 0.000000000000000000 ) ) ;
#10436=FILL_AREA_STYLE_COLOUR ( '', #11640 ) ;
#10466=CARTESIAN_POINT ( 'NONE',  ( -5.196152422706636465, 9.000000000000001776, 5.000000000000000000 ) ) ;
#10495=DIRECTION ( 'NONE',  ( -0.000000000000000000, -0.000000000000000000, -1.000000000000000000 ) ) ;
#10505=DIRECTION ( 'NONE',  ( -1.000000000000000000, -1.669238443041287429E-16, 0.000000000000000000 ) ) ;
#10519=DIRECTION ( 'NONE',  ( 0.4999999999999997224, 0.8660254037844387076, 0.000000000000000000 ) ) ;
#10548=PRODUCT ( 'nut M10', 'nut M10', '', ( #14394 ) ) ;
#10563=CARTESIAN_POINT ( 'NONE',  ( -5.196152422706636465, 9.000000000000001776, 5.000000000000000000 ) ) ;
#10572=EDGE_CURVE ( 'NONE', #15023, #927, #13919, .T. ) ;
#10701=( NAMED_UNIT ( * ) SI_UNIT ( $, .STERADIAN. ) SOLID_ANGLE_UNIT ( ) );
#10726=CARTESIAN_POINT ( 'NONE',  ( 5.196152422706632024, 9.000000000000003553, 5.000000000000000000 ) ) ;
#10988=DIRECTION ( 'NONE',  ( -0.5000000000000001110, 0.8660254037844385966, 0.000000000000000000 ) ) ;
#11071=VERTEX_POINT ( 'NONE', #6022 ) ;
#11078=CARTESIAN_POINT ( 'NONE',  ( -5.196152422706636465, 9.000000000000001776, 0.000000000000000000 ) ) ;
#11083=DIRECTION ( 'NONE',  ( -0.4999999999999999445, 0.8660254037844385966, 0.000000000000000000 ) ) ;
#11144=AXIS2_PLACEMENT_3D ( 'NONE', #12537, #10113, #5530 ) ;
#11166=CARTESIAN_POINT ( 'NONE',  ( 10.39230484541326582, 0.000000000000000000, 5.000000000000000000 ) ) ;
#11171=AXIS2_PLACEMENT_3D ( 'NONE', #4966, #14501, #195 ) ;
#11209=ORIENTED_EDGE ( 'NONE', *, *, #1670, .T. ) ;
#11225=ORIENTED_EDGE ( 'NONE', *, *, #8173, .T. ) ;
#11238=ORIENTED_EDGE ( 'NONE', *, *, #6243, .F. ) ;
#11266=ADVANCED_FACE ( 'NONE', ( #4323 ), #7686, .F. ) ;
#11331=DIRECTION ( 'NONE',  ( -1.000000000000000000, 0.000000000000000000, 0.000000000000000000 ) ) ;
#11362=UNCERTAINTY_MEASURE_WITH_UNIT (LENGTH_MEASURE( 1.000000000000000082E-05 ), #1061, 'distance_accuracy_value', 'NONE');
#11378=VECTOR ( 'NONE', #3734, 1000.000000000000000 ) ;
#11433=CARTESIAN_POINT ( 'NONE',  ( 0.000000000000000000, 0.000000000000000000, 0.000000000000000000 ) ) ;
#11498=DIRECTION ( 'NONE',  ( 1.000000000000000000, 0.000000000000000000, 0.000000000000000000 ) ) ;
#11543=VERTEX_POINT ( 'NONE', #3987 ) ;
#11560=CARTESIAN_POINT ( 'NONE',  ( -5.000000000000000000, 0.000000000000000000, 5.000000000000000000 ) ) ;
#11640=COLOUR_RGB ( '', 0.31764706, 0.68627451, 0.89019608) ;
#11691=PRODUCT_DEFINITION_SHAPE ( 'NONE', 'NONE',  #5848 ) ;
#11699=PRESENTATION_STYLE_ASSIGNMENT (( #14939 ) ) ;
#11731=VERTEX_POINT ( 'NONE', #12667 ) ;
#11800=CARTESIAN_POINT ( 'NONE',  ( 5.196152422706632024, 9.000000000000003553, 0.000000000000000000 ) ) ;
#11872=CARTESIAN_POINT ( 'NONE',  ( -10.39230484541326582, 4.570335331080236228E-16, 5.000000000000000000 ) ) ;
#11889=ORIENTED_EDGE ( 'NONE', *, *, #5899, .F. ) ;
#11930=VECTOR ( 'NONE', #10505, 1000.000000000000000 ) ;
#11996=FACE_BOUND ( 'NONE', #1863, .T. ) ;
#12204=EDGE_CURVE ( 'NONE', #11543, #6413, #7064, .T. ) ;
#12214=CARTESIAN_POINT ( 'NONE',  ( -5.196152422706630247, -9.000000000000005329, 0.000000000000000000 ) ) ;
#12314=DIRECTION ( 'NONE',  ( 0.4999999999999997224, 0.8660254037844387076, 0.000000000000000000 ) ) ;
#12316=AXIS2_PLACEMENT_3D ( 'NONE', #6932, #1067, #8354 ) ;
#12337=AXIS2_PLACEMENT_3D ( 'NONE', #4568, #8147, #5681 ) ;
#12342=ORIENTED_EDGE ( 'NONE', *, *, #9225, .T. ) ;
#12361=EDGE_CURVE ( 'NONE', #3648, #6413, #2787, .T. ) ;
#12442=ORIENTED_EDGE ( 'NONE', *, *, #12204, .T. ) ;
#12465=PLANE ( 'NONE',  #11144 ) ;
#12476=EDGE_LOOP ( 'NONE', ( #7632, #11209, #14343, #2138, #8532, #12342 ) ) ;
#12507=DIRECTION ( 'NONE',  ( -0.000000000000000000, -0.000000000000000000, -1.000000000000000000 ) ) ;
#12537=CARTESIAN_POINT ( 'NONE',  ( 5.196152422706632024, 9.000000000000003553, 5.000000000000000000 ) ) ;
#12546=SHAPE_REPRESENTATION ( 'nut M10', ( #12337 ), #9054 ) ;
#12559=ORIENTED_EDGE ( 'NONE', *, *, #948, .T. ) ;
#12625=CARTESIAN_POINT ( 'NONE',  ( -5.196152422706630247, -9.000000000000005329, 5.000000000000000000 ) ) ;
#12667=CARTESIAN_POINT ( 'NONE',  ( -5.196152422706630247, -9.000000000000005329, 5.000000000000000000 ) ) ;
#12686=APPLICATION_CONTEXT ( 'automotive_design' ) ;
#12818=FACE_BOUND ( 'NONE', #2467, .T. ) ;
#12866=DIRECTION ( 'NONE',  ( -1.000000000000000000, -1.669238443041287922E-16, 0.000000000000000000 ) ) ;
#12879=FACE_OUTER_BOUND ( 'NONE', #1533, .T. ) ;
#12919=DIRECTION ( 'NONE',  ( 0.4999999999999997224, 0.8660254037844387076, 0.000000000000000000 ) ) ;
#12977=SHAPE_REPRESENTATION_RELATIONSHIP ( 'NONE' , 'NONE' ,  #12546, #6616 ) ;
#13016=ORIENTED_EDGE ( 'NONE', *, *, #7680, .T. ) ;
#13077=ORIENTED_EDGE ( 'NONE', *, *, #5171, .T. ) ;
#13401=CARTESIAN_POINT ( 'NONE',  ( 5.196152422706635576, -9.000000000000003553, 5.000000000000000000 ) ) ;
#13417=AXIS2_PLACEMENT_3D ( 'NONE', #14292, #3487, #2305 ) ;
#13521=SURFACE_SIDE_STYLE ('',( #15227 ) ) ;
#13625=LINE ( 'NONE', #1708, #7095 ) ;
#13669=ORIENTED_EDGE ( 'NONE', *, *, #6930, .T. ) ;
#13690=CYLINDRICAL_SURFACE ( 'NONE', #5903, 5.000000000000000000 ) ;
#13755=CARTESIAN_POINT ( 'NONE',  ( -5.196152422706630247, -9.000000000000005329, 0.000000000000000000 ) ) ;
#13765=ORIENTED_EDGE ( 'NONE', *, *, #8253, .F. ) ;
#13828=VERTEX_POINT ( 'NONE', #10563 ) ;
#13878=DIRECTION ( 'NONE',  ( 0.000000000000000000, 0.000000000000000000, 1.000000000000000000 ) ) ;
#13897=DIRECTION ( 'NONE',  ( 0.000000000000000000, 0.000000000000000000, 1.000000000000000000 ) ) ;
#13919=CIRCLE ( 'NONE', #286, 5.000000000000000000 ) ;
#13937=( NAMED_UNIT ( * ) PLANE_ANGLE_UNIT ( ) SI_UNIT ( $, .RADIAN. ) );
#14037=ORIENTED_EDGE ( 'NONE', *, *, #10572, .F. ) ;
#14054=ORIENTED_EDGE ( 'NONE', *, *, #9637, .F. ) ;
#14080=PLANE ( 'NONE',  #9064 ) ;
#14123=EDGE_LOOP ( 'NONE', ( #7551, #2853, #1747, #13077 ) ) ;
#14173=CARTESIAN_POINT ( 'NONE',  ( 5.196152422706635576, -9.000000000000003553, 5.000000000000000000 ) ) ;
#14184=CARTESIAN_POINT ( 'NONE',  ( 0.000000000000000000, 0.000000000000000000, 5.000000000000000000 ) ) ;
#14203=CARTESIAN_POINT ( 'NONE',  ( 5.196152422706632024, 9.000000000000003553, 0.000000000000000000 ) ) ;
#14239=ORIENTED_EDGE ( 'NONE', *, *, #4833, .F. ) ;
#14255=AXIS2_PLACEMENT_3D ( 'NONE', #11166, #8796, #9988 ) ;
#14292=CARTESIAN_POINT ( 'NONE',  ( 5.196152422706635576, -9.000000000000003553, 5.000000000000000000 ) ) ;
#14341=DIRECTION ( 'NONE',  ( -0.000000000000000000, -0.000000000000000000, -1.000000000000000000 ) ) ;
#14343=ORIENTED_EDGE ( 'NONE', *, *, #8253, .T. ) ;
#14394=PRODUCT_CONTEXT ( 'NONE', #5878, 'mechanical' ) ;
#14421=ORIENTED_EDGE ( 'NONE', *, *, #1670, .F. ) ;
#14501=DIRECTION ( 'NONE',  ( 0.000000000000000000, -0.000000000000000000, 1.000000000000000000 ) ) ;
#14543=VERTEX_POINT ( 'NONE', #8123 ) ;
#14553=ORIENTED_EDGE ( 'NONE', *, *, #8173, .F. ) ;
#14576=CARTESIAN_POINT ( 'NONE',  ( 5.196152422706635576, -9.000000000000003553, 0.000000000000000000 ) ) ;
#14608=VECTOR ( 'NONE', #9989, 1000.000000000000000 ) ;
#14658=EDGE_CURVE ( 'NONE', #927, #15023, #1735, .T. ) ;
#14676=CLOSED_SHELL ( 'NONE', ( #11266, #7266, #135, #7983, #3508, #10009, #1878, #4109, #513, #6072 ) ) ;
#14772=ORIENTED_EDGE ( 'NONE', *, *, #2996, .T. ) ;
#14825=AXIS2_PLACEMENT_3D ( 'NONE', #7133, #1032, #10988 ) ;
#14859=DIRECTION ( 'NONE',  ( -1.669238443041287922E-16, 1.000000000000000000, 0.000000000000000000 ) ) ;
#14939=SURFACE_STYLE_USAGE ( .BOTH. , #13521 ) ;
#15000=ORIENTED_EDGE ( 'NONE', *, *, #7569, .F. ) ;
#15023=VERTEX_POINT ( 'NONE', #11560 ) ;
#15083=CARTESIAN_POINT ( 'NONE',  ( 10.39230484541326582, 0.000000000000000000, 5.000000000000000000 ) ) ;
#15096=UNCERTAINTY_MEASURE_WITH_UNIT (LENGTH_MEASURE( 1.000000000000000082E-05 ), #10146, 'distance_accuracy_value', 'NONE');
#15138=FACE_OUTER_BOUND ( 'NONE', #9516, .T. ) ;
#15224=AXIS2_PLACEMENT_3D ( 'NONE', #14184, #10495, #2115 ) ;
#15227=SURFACE_STYLE_FILL_AREA ( #5618 ) ;
#15253=DIRECTION ( 'NONE',  ( -0.4999999999999997224, -0.8660254037844388186, 0.000000000000000000 ) ) ;
#15267=CARTESIAN_POINT ( 'NONE',  ( 10.39230484541326582, 0.000000000000000000, 5.000000000000000000 ) ) ;
#15285=ORIENTED_EDGE ( 'NONE', *, *, #2223, .F. ) ;
#15341=VECTOR ( 'NONE', #812, 1000.000000000000000 ) ;
#15343=CARTESIAN_POINT ( 'NONE',  ( -5.000000000000000000, 0.000000000000000000, 0.000000000000000000 ) ) ;
#15549=DIRECTION ( 'NONE',  ( -0.000000000000000000, -0.000000000000000000, -1.000000000000000000 ) ) ;
ENDSEC;
END-ISO-10303-21;
